ISO-10303-21;
HEADER;
FILE_DESCRIPTION (('STEP AP214'),
    '1' );
FILE_NAME ('HOLDING PLATE.step',
    '2026-10-09T16:01:55',
    ( '' ),
    ( '' ),
    'SwSTEP 2.0',
    'SolidWorks 2024',
    '' );
FILE_SCHEMA (( 'AUTOMOTIVE_DESIGN' ));
ENDSEC;

DATA;
#184=( LENGTH_UNIT ( ) NAMED_UNIT ( * ) SI_UNIT ( .MILLI., .METRE. ) );
#220=PLANE ( 'NONE',  #66350 ) ;
#305=DIRECTION ( 'NONE',  ( -1.000000000000000000, -0.000000000000000000, -0.000000000000000000 ) ) ;
#637=SURFACE_STYLE_FILL_AREA ( #1652 ) ;
#796=DIRECTION ( 'NONE',  ( 0.000000000000000000, -1.000000000000000000, 0.000000000000000000 ) ) ;
#838=AXIS2_PLACEMENT_3D ( 'NONE', #32473, #4555, #64989 ) ;
#1054=ORIENTED_EDGE ( 'NONE', *, *, #39987, .F. ) ;
#1170=ORIENTED_EDGE ( 'NONE', *, *, #7468, .F. ) ;
#1200=VERTEX_POINT ( 'NONE', #41012 ) ;
#1221=ORIENTED_EDGE ( 'NONE', *, *, #59660, .F. ) ;
#1231=VERTEX_POINT ( 'NONE', #56925 ) ;
#1289=ORIENTED_EDGE ( 'NONE', *, *, #15089, .F. ) ;
#1391=VERTEX_POINT ( 'NONE', #22592 ) ;
#1457=DIRECTION ( 'NONE',  ( -0.000000000000000000, -0.000000000000000000, 1.000000000000000000 ) ) ;
#1652=FILL_AREA_STYLE ('',( #61043 ) ) ;
#1668=CARTESIAN_POINT ( 'NONE',  ( 181.4833316329832940, 9.000000000000001776, 284.4801873289890182 ) ) ;
#1766=AXIS2_PLACEMENT_3D ( 'NONE', #18824, #40392, #23778 ) ;
#1866=VECTOR ( 'NONE', #43487, 1000.000000000000000 ) ;
#2065=PRODUCT_DEFINITION_CONTEXT ( 'detailed design', #64814, 'design' ) ;
#2152=CIRCLE ( 'NONE', #66502, 2.215251240775983899 ) ;
#2342=LINE ( 'NONE', #22869, #3348 ) ;
#2493=CARTESIAN_POINT ( 'NONE',  ( 146.5599459900709860, 9.000000000000001776, 328.5239988703752942 ) ) ;
#2538=DIRECTION ( 'NONE',  ( -0.000000000000000000, -1.000000000000000000, -0.000000000000000000 ) ) ;
#2682=ORIENTED_EDGE ( 'NONE', *, *, #6452, .T. ) ;
#2719=DIRECTION ( 'NONE',  ( 0.000000000000000000, 0.000000000000000000, 1.000000000000000000 ) ) ;
#2742=EDGE_LOOP ( 'NONE', ( #8520, #22275, #56894, #42174 ) ) ;
#2757=ADVANCED_FACE ( 'NONE', ( #29631 ), #51204, .F. ) ;
#2806=VERTEX_POINT ( 'NONE', #13725 ) ;
#2897=AXIS2_PLACEMENT_3D ( 'NONE', #27773, #17851, #11491 ) ;
#2967=AXIS2_PLACEMENT_3D ( 'NONE', #30549, #9688, #25246 ) ;
#3052=VERTEX_POINT ( 'NONE', #30923 ) ;
#3094=DIRECTION ( 'NONE',  ( 0.000000000000000000, 0.000000000000000000, 1.000000000000000000 ) ) ;
#3177=FACE_OUTER_BOUND ( 'NONE', #25310, .T. ) ;
#3181=ORIENTED_EDGE ( 'NONE', *, *, #35327, .T. ) ;
#3315=CARTESIAN_POINT ( 'NONE',  ( 151.5599459900709860, -10.00000000000000178, 282.8454385697650082 ) ) ;
#3348=VECTOR ( 'NONE', #6942, 1000.000000000000000 ) ;
#3418=VECTOR ( 'NONE', #30647, 1000.000000000000000 ) ;
#3589=CARTESIAN_POINT ( 'NONE',  ( 146.5599459900709860, 9.000000000000001776, 280.7801873289890295 ) ) ;
#4286=FACE_OUTER_BOUND ( 'NONE', #66115, .T. ) ;
#4428=EDGE_CURVE ( 'NONE', #48708, #33185, #43902, .T. ) ;
#4486=CARTESIAN_POINT ( 'NONE',  ( 176.4833316329832940, -10.00000000000000178, 326.8892501111512843 ) ) ;
#4555=DIRECTION ( 'NONE',  ( 0.000000000000000000, -1.000000000000000000, 0.000000000000000000 ) ) ;
#4635=DIRECTION ( 'NONE',  ( 0.000000000000000000, 0.000000000000000000, -1.000000000000000000 ) ) ;
#4798=EDGE_LOOP ( 'NONE', ( #14111, #15823, #10542, #22744 ) ) ;
#4982=EDGE_CURVE ( 'NONE', #17940, #67565, #23287, .T. ) ;
#5156=DIRECTION ( 'NONE',  ( -1.000000000000000000, 0.000000000000000000, 0.000000000000000000 ) ) ;
#5341=ORIENTED_EDGE ( 'NONE', *, *, #64622, .F. ) ;
#5484=EDGE_CURVE ( 'NONE', #16384, #1200, #34848, .T. ) ;
#5670=DIRECTION ( 'NONE',  ( 0.000000000000000000, -1.000000000000000000, 0.000000000000000000 ) ) ;
#5739=LINE ( 'NONE', #27305, #33742 ) ;
#5801=VECTOR ( 'NONE', #8883, 1000.000000000000000 ) ;
#5829=ORIENTED_EDGE ( 'NONE', *, *, #39275, .F. ) ;
#6081=DIRECTION ( 'NONE',  ( -0.000000000000000000, 1.000000000000000000, -0.000000000000000000 ) ) ;
#6113=ORIENTED_EDGE ( 'NONE', *, *, #12728, .F. ) ;
#6234=EDGE_LOOP ( 'NONE', ( #33654, #29606 ) ) ;
#6279=PRESENTATION_STYLE_ASSIGNMENT (( #66007 ) ) ;
#6385=DIRECTION ( 'NONE',  ( 0.000000000000000000, -1.000000000000000000, 0.000000000000000000 ) ) ;
#6452=EDGE_CURVE ( 'NONE', #30313, #45034, #68892, .T. ) ;
#6654=DIRECTION ( 'NONE',  ( 0.000000000000000000, -1.000000000000000000, 0.000000000000000000 ) ) ;
#6881=EDGE_CURVE ( 'NONE', #54084, #17940, #52188, .T. ) ;
#6931=ORIENTED_EDGE ( 'NONE', *, *, #41406, .T. ) ;
#6942=DIRECTION ( 'NONE',  ( -0.000000000000000000, -1.000000000000000000, -0.000000000000000000 ) ) ;
#7096=FACE_BOUND ( 'NONE', #16177, .T. ) ;
#7203=FACE_OUTER_BOUND ( 'NONE', #67307, .T. ) ;
#7323=CARTESIAN_POINT ( 'NONE',  ( 176.4833316329832940, 9.000000000000001776, 280.6301873289890523 ) ) ;
#7468=EDGE_CURVE ( 'NONE', #58210, #19830, #23623, .T. ) ;
#7481=ORIENTED_EDGE ( 'NONE', *, *, #53672, .T. ) ;
#7671=CARTESIAN_POINT ( 'NONE',  ( 151.5599459900709860, -10.00000000000000178, 324.6739988703752715 ) ) ;
#7688=EDGE_CURVE ( 'NONE', #45034, #16384, #2342, .T. ) ;
#7751=EDGE_CURVE ( 'NONE', #19830, #52952, #12933, .T. ) ;
#7762=ORIENTED_EDGE ( 'NONE', *, *, #69483, .F. ) ;
#7807=DIRECTION ( 'NONE',  ( 0.000000000000000000, 0.000000000000000000, -1.000000000000000000 ) ) ;
#7846=LINE ( 'NONE', #62645, #52811 ) ;
#7888=CIRCLE ( 'NONE', #14674, 2.215251240775983899 ) ;
#7934=CARTESIAN_POINT ( 'NONE',  ( 176.4833316329832940, -10.00000000000000178, 322.4587476295993156 ) ) ;
#8009=LINE ( 'NONE', #29582, #52301 ) ;
#8095=CLOSED_SHELL ( 'NONE', ( #53061, #59530, #52570, #51828, #19357, #45008, #8879, #67806, #8113, #55752, #43523, #15975, #19612, #14433, #44856, #13090, #27181, #2757 ) ) ;
#8113=ADVANCED_FACE ( 'NONE', ( #7203 ), #45037, .F. ) ;
#8215=AXIS2_PLACEMENT_3D ( 'NONE', #27534, #6654, #55448 ) ;
#8269=DIRECTION ( 'NONE',  ( 0.000000000000000000, 0.000000000000000000, 1.000000000000000000 ) ) ;
#8432=ORIENTED_EDGE ( 'NONE', *, *, #7688, .T. ) ;
#8456=DIRECTION ( 'NONE',  ( 0.000000000000000000, 1.000000000000000000, 0.000000000000000000 ) ) ;
#8520=ORIENTED_EDGE ( 'NONE', *, *, #45954, .T. ) ;
#8538=VERTEX_POINT ( 'NONE', #43922 ) ;
#8663=CIRCLE ( 'NONE', #15438, 2.215251240775983899 ) ;
#8786=VECTOR ( 'NONE', #56118, 1000.000000000000000 ) ;
#8864=CARTESIAN_POINT ( 'NONE',  ( 151.5599459900709860, -10.00000000000000178, 280.6301873289890523 ) ) ;
#8879=ADVANCED_FACE ( 'NONE', ( #36448 ), #15935, .F. ) ;
#8880=DIRECTION ( 'NONE',  ( 0.000000000000000000, 1.000000000000000000, 0.000000000000000000 ) ) ;
#8883=DIRECTION ( 'NONE',  ( -1.000000000000000000, -0.000000000000000000, -0.000000000000000000 ) ) ;
#8895=DIRECTION ( 'NONE',  ( 0.000000000000000000, -1.000000000000000000, 0.000000000000000000 ) ) ;
#9275=ORIENTED_EDGE ( 'NONE', *, *, #23032, .T. ) ;
#9324=ORIENTED_EDGE ( 'NONE', *, *, #11954, .F. ) ;
#9688=DIRECTION ( 'NONE',  ( 0.000000000000000000, 1.000000000000000000, -0.000000000000000000 ) ) ;
#10120=AXIS2_PLACEMENT_3D ( 'NONE', #35027, #14171, #7807 ) ;
#10542=ORIENTED_EDGE ( 'NONE', *, *, #6881, .T. ) ;
#10920=EDGE_CURVE ( 'NONE', #16796, #3052, #17457, .T. ) ;
#10949=VECTOR ( 'NONE', #18920, 1000.000000000000000 ) ;
#10970=DIRECTION ( 'NONE',  ( 0.000000000000000000, 0.000000000000000000, -1.000000000000000000 ) ) ;
#10972=CARTESIAN_POINT ( 'NONE',  ( 176.4833316329832940, -10.00000000000000178, 282.8454385697650082 ) ) ;
#11037=FACE_BOUND ( 'NONE', #27565, .T. ) ;
#11288=AXIS2_PLACEMENT_3D ( 'NONE', #16911, #28541, #32820 ) ;
#11375=VECTOR ( 'NONE', #26813, 1000.000000000000000 ) ;
#11491=DIRECTION ( 'NONE',  ( -1.000000000000000000, 0.000000000000000000, -0.000000000000000000 ) ) ;
#11623=AXIS2_PLACEMENT_3D ( 'NONE', #66429, #49821, #24341 ) ;
#11668=LINE ( 'NONE', #33254, #38330 ) ;
#11825=LINE ( 'NONE', #22462, #14376 ) ;
#11835=CIRCLE ( 'NONE', #34385, 2.215251240775983899 ) ;
#11929=VECTOR ( 'NONE', #39761, 1000.000000000000000 ) ;
#11954=EDGE_CURVE ( 'NONE', #39907, #1200, #43605, .T. ) ;
#12084=ORIENTED_EDGE ( 'NONE', *, *, #6452, .F. ) ;
#12159=( NAMED_UNIT ( * ) SI_UNIT ( $, .STERADIAN. ) SOLID_ANGLE_UNIT ( ) );
#12170=CARTESIAN_POINT ( 'NONE',  ( 146.5599459900709860, 9.000000000000001776, 284.4801873289890182 ) ) ;
#12255=SURFACE_SIDE_STYLE ('',( #637 ) ) ;
#12433=CARTESIAN_POINT ( 'NONE',  ( 151.5599459900709860, 9.000000000000001776, 282.8454385697650082 ) ) ;
#12728=EDGE_CURVE ( 'NONE', #16384, #37841, #42041, .T. ) ;
#12836=CIRCLE ( 'NONE', #33204, 2.215251240775983899 ) ;
#12933=LINE ( 'NONE', #10972, #46294 ) ;
#12956=ORIENTED_EDGE ( 'NONE', *, *, #22230, .F. ) ;
#12957=AXIS2_PLACEMENT_3D ( 'NONE', #18440, #46033, #66551 ) ;
#13037=AXIS2_PLACEMENT_3D ( 'NONE', #7671, #50807, #2719 ) ;
#13074=EDGE_CURVE ( 'NONE', #65968, #1391, #51519, .T. ) ;
#13090=ADVANCED_FACE ( 'NONE', ( #62110 ), #30305, .F. ) ;
#13161=DIRECTION ( 'NONE',  ( 0.000000000000000000, -1.000000000000000000, 0.000000000000000000 ) ) ;
#13369=EDGE_CURVE ( 'NONE', #61801, #63673, #36483, .T. ) ;
#13483=LINE ( 'NONE', #3589, #18139 ) ;
#13725=CARTESIAN_POINT ( 'NONE',  ( 146.5599459900709860, 9.000000000000001776, 276.7801873289890295 ) ) ;
#13771=FACE_BOUND ( 'NONE', #50801, .T. ) ;
#13848=CARTESIAN_POINT ( 'NONE',  ( 176.4833316329832940, 9.000000000000001776, 322.4587476295993156 ) ) ;
#13917=FACE_OUTER_BOUND ( 'NONE', #60692, .T. ) ;
#14111=ORIENTED_EDGE ( 'NONE', *, *, #61802, .T. ) ;
#14171=DIRECTION ( 'NONE',  ( 0.000000000000000000, -1.000000000000000000, 0.000000000000000000 ) ) ;
#14224=ORIENTED_EDGE ( 'NONE', *, *, #13074, .T. ) ;
#14233=VECTOR ( 'NONE', #1457, 1000.000000000000000 ) ;
#14376=VECTOR ( 'NONE', #59932, 1000.000000000000000 ) ;
#14433=ADVANCED_FACE ( 'NONE', ( #26071 ), #42667, .T. ) ;
#14485=PLANE ( 'NONE',  #20594 ) ;
#14599=ORIENTED_EDGE ( 'NONE', *, *, #4982, .F. ) ;
#14674=AXIS2_PLACEMENT_3D ( 'NONE', #44462, #38494, #60734 ) ;
#14895=ORIENTED_EDGE ( 'NONE', *, *, #39271, .F. ) ;
#15089=EDGE_CURVE ( 'NONE', #67565, #59771, #27258, .T. ) ;
#15209=VECTOR ( 'NONE', #64156, 1000.000000000000000 ) ;
#15299=CARTESIAN_POINT ( 'NONE',  ( 176.4833316329832940, 9.000000000000001776, 324.6739988703752715 ) ) ;
#15438=AXIS2_PLACEMENT_3D ( 'NONE', #42107, #8880, #30454 ) ;
#15502=ORIENTED_EDGE ( 'NONE', *, *, #42629, .T. ) ;
#15823=ORIENTED_EDGE ( 'NONE', *, *, #63993, .T. ) ;
#15935=PLANE ( 'NONE',  #25204 ) ;
#15975=ADVANCED_FACE ( 'NONE', ( #53973, #48659, #16482 ), #220, .F. ) ;
#16177=EDGE_LOOP ( 'NONE', ( #31195, #62976 ) ) ;
#16190=EDGE_CURVE ( 'NONE', #33185, #67565, #7846, .T. ) ;
#16216=CARTESIAN_POINT ( 'NONE',  ( 146.5599459900709860, 5.000000000000000000, 320.8239988703753056 ) ) ;
#16384=VERTEX_POINT ( 'NONE', #44207 ) ;
#16439=SHAPE_REPRESENTATION_RELATIONSHIP ( 'NONE' , 'NONE' ,  #62481, #28414 ) ;
#16482=FACE_OUTER_BOUND ( 'NONE', #42699, .T. ) ;
#16499=CARTESIAN_POINT ( 'NONE',  ( 151.5599459900709860, 0.000000000000000000, 278.4149360882130395 ) ) ;
#16708=ORIENTED_EDGE ( 'NONE', *, *, #5484, .T. ) ;
#16747=CARTESIAN_POINT ( 'NONE',  ( 181.4833316329832940, 9.000000000000001776, 284.4801873289890182 ) ) ;
#16796=VERTEX_POINT ( 'NONE', #51965 ) ;
#16846=CIRCLE ( 'NONE', #68787, 2.215251240775983899 ) ;
#16911=CARTESIAN_POINT ( 'NONE',  ( 151.5599459900709860, 9.000000000000001776, 280.6301873289890523 ) ) ;
#16936=EDGE_CURVE ( 'NONE', #52952, #1231, #12836, .T. ) ;
#17040=ORIENTED_EDGE ( 'NONE', *, *, #65712, .F. ) ;
#17167=ORIENTED_EDGE ( 'NONE', *, *, #67397, .T. ) ;
#17179=CARTESIAN_POINT ( 'NONE',  ( 176.4833316329832940, 9.000000000000001776, 326.8892501111512843 ) ) ;
#17443=ORIENTED_EDGE ( 'NONE', *, *, #13369, .F. ) ;
#17457=CIRCLE ( 'NONE', #69410, 2.215251240775983899 ) ;
#17851=DIRECTION ( 'NONE',  ( 0.000000000000000000, 0.000000000000000000, -1.000000000000000000 ) ) ;
#17916=FACE_OUTER_BOUND ( 'NONE', #35326, .T. ) ;
#17940=VERTEX_POINT ( 'NONE', #19184 ) ;
#18139=VECTOR ( 'NONE', #26909, 1000.000000000000000 ) ;
#18189=AXIS2_PLACEMENT_3D ( 'NONE', #69541, #26762, #43008 ) ;
#18440=CARTESIAN_POINT ( 'NONE',  ( 146.5599459900709860, 9.000000000000001776, 320.8239988703753056 ) ) ;
#18567=EDGE_LOOP ( 'NONE', ( #38086, #37911, #49770, #55962 ) ) ;
#18689=MECHANICAL_DESIGN_GEOMETRIC_PRESENTATION_REPRESENTATION('',(#52752),#22250);
#18824=CARTESIAN_POINT ( 'NONE',  ( 176.4833316329832940, -10.00000000000000178, 324.6739988703752715 ) ) ;
#18850=COLOUR_RGB ( '', 0.66274510, 0.83137255, 0.94901961) ;
#18920=DIRECTION ( 'NONE',  ( -0.000000000000000000, -0.000000000000000000, -1.000000000000000000 ) ) ;
#19184=CARTESIAN_POINT ( 'NONE',  ( 146.5599459900709860, 0.000000000000000000, 276.7801873289890295 ) ) ;
#19300=CARTESIAN_POINT ( 'NONE',  ( 181.4833316329832940, 9.000000000000001776, 276.7801873289890295 ) ) ;
#19304=MANIFOLD_SOLID_BREP ( 'Cut-Extrude1', #8095 ) ;
#19357=ADVANCED_FACE ( 'NONE', ( #17916 ), #48725, .F. ) ;
#19612=ADVANCED_FACE ( 'NONE', ( #48996 ), #27074, .T. ) ;
#19723=CARTESIAN_POINT ( 'NONE',  ( 181.4833316329832940, 9.000000000000001776, 328.5239988703752942 ) ) ;
#19747=ORIENTED_EDGE ( 'NONE', *, *, #46543, .F. ) ;
#19766=DIRECTION ( 'NONE',  ( 0.000000000000000000, 1.000000000000000000, 0.000000000000000000 ) ) ;
#19830=VERTEX_POINT ( 'NONE', #28793 ) ;
#20007=EDGE_LOOP ( 'NONE', ( #44571, #67579 ) ) ;
#20250=CYLINDRICAL_SURFACE ( 'NONE', #39962, 2.215251240775983899 ) ;
#20316=CARTESIAN_POINT ( 'NONE',  ( 146.5599459900709860, 9.000000000000001776, 284.4801873289890182 ) ) ;
#20594=AXIS2_PLACEMENT_3D ( 'NONE', #46295, #19766, #41342 ) ;
#20705=EDGE_LOOP ( 'NONE', ( #53460, #57926, #45303, #60477 ) ) ;
#20747=DIRECTION ( 'NONE',  ( 1.000000000000000000, 0.000000000000000000, -0.000000000000000000 ) ) ;
#20790=CARTESIAN_POINT ( 'NONE',  ( 181.4833316329832940, 9.000000000000001776, 324.5239988703752942 ) ) ;
#20970=CARTESIAN_POINT ( 'NONE',  ( 151.5599459900709860, 0.000000000000000000, 280.6301873289890523 ) ) ;
#21030=LINE ( 'NONE', #38346, #24322 ) ;
#21037=VECTOR ( 'NONE', #37178, 1000.000000000000000 ) ;
#21432=DIRECTION ( 'NONE',  ( 0.000000000000000000, -1.000000000000000000, 0.000000000000000000 ) ) ;
#21579=ORIENTED_EDGE ( 'NONE', *, *, #44661, .F. ) ;
#21653=CARTESIAN_POINT ( 'NONE',  ( 0.000000000000000000, 0.000000000000000000, 0.000000000000000000 ) ) ;
#21847=( NAMED_UNIT ( * ) PLANE_ANGLE_UNIT ( ) SI_UNIT ( $, .RADIAN. ) );
#22166=DIRECTION ( 'NONE',  ( -0.000000000000000000, 1.000000000000000000, -0.000000000000000000 ) ) ;
#22207=( NAMED_UNIT ( * ) SI_UNIT ( $, .STERADIAN. ) SOLID_ANGLE_UNIT ( ) );
#22230=EDGE_CURVE ( 'NONE', #3052, #16796, #56060, .T. ) ;
#22250=( GEOMETRIC_REPRESENTATION_CONTEXT ( 3 ) GLOBAL_UNCERTAINTY_ASSIGNED_CONTEXT ( ( #27407 ) ) GLOBAL_UNIT_ASSIGNED_CONTEXT ( ( #64992, #21847, #22207 ) ) REPRESENTATION_CONTEXT ( 'NONE', 'WORKASPACE' ) );
#22275=ORIENTED_EDGE ( 'NONE', *, *, #13369, .T. ) ;
#22462=CARTESIAN_POINT ( 'NONE',  ( 146.5599459900709860, 9.000000000000001776, 276.7801873289890295 ) ) ;
#22486=CARTESIAN_POINT ( 'NONE',  ( 0.000000000000000000, 9.000000000000001776, 0.000000000000000000 ) ) ;
#22511=DIRECTION ( 'NONE',  ( 0.000000000000000000, 0.000000000000000000, 1.000000000000000000 ) ) ;
#22548=DIRECTION ( 'NONE',  ( 0.000000000000000000, -1.000000000000000000, 0.000000000000000000 ) ) ;
#22592=CARTESIAN_POINT ( 'NONE',  ( 151.5599459900709860, 9.000000000000001776, 278.4149360882130395 ) ) ;
#22744=ORIENTED_EDGE ( 'NONE', *, *, #55725, .T. ) ;
#22775=CARTESIAN_POINT ( 'NONE',  ( 0.000000000000000000, 0.000000000000000000, 0.000000000000000000 ) ) ;
#22869=CARTESIAN_POINT ( 'NONE',  ( 181.4833316329832940, 9.000000000000001776, 320.8239988703753056 ) ) ;
#23032=EDGE_CURVE ( 'NONE', #39907, #26623, #40476, .T. ) ;
#23097=AXIS2_PLACEMENT_3D ( 'NONE', #8864, #41392, #35025 ) ;
#23265=ORIENTED_EDGE ( 'NONE', *, *, #64622, .T. ) ;
#23287=LINE ( 'NONE', #44850, #33364 ) ;
#23366=CIRCLE ( 'NONE', #838, 2.215251240775983899 ) ;
#23425=PLANE ( 'NONE',  #12957 ) ;
#23464=DIRECTION ( 'NONE',  ( 0.000000000000000000, 0.000000000000000000, -1.000000000000000000 ) ) ;
#23579=LINE ( 'NONE', #29932, #8786 ) ;
#23623=CIRCLE ( 'NONE', #10120, 2.215251240775983899 ) ;
#23778=DIRECTION ( 'NONE',  ( 0.000000000000000000, 0.000000000000000000, 1.000000000000000000 ) ) ;
#24322=VECTOR ( 'NONE', #23464, 1000.000000000000000 ) ;
#24335=ORIENTED_EDGE ( 'NONE', *, *, #5484, .F. ) ;
#24341=DIRECTION ( 'NONE',  ( 0.000000000000000000, 0.000000000000000000, 1.000000000000000000 ) ) ;
#24554=ORIENTED_EDGE ( 'NONE', *, *, #35327, .F. ) ;
#24866=EDGE_CURVE ( 'NONE', #63673, #66056, #16846, .T. ) ;
#24990=EDGE_CURVE ( 'NONE', #56861, #16796, #5739, .T. ) ;
#24991=DIRECTION ( 'NONE',  ( 0.000000000000000000, 1.000000000000000000, 0.000000000000000000 ) ) ;
#25036=ORIENTED_EDGE ( 'NONE', *, *, #63993, .F. ) ;
#25050=APPLICATION_CONTEXT ( 'automotive_design' ) ;
#25204=AXIS2_PLACEMENT_3D ( 'NONE', #58018, #69692, #4635 ) ;
#25246=DIRECTION ( 'NONE',  ( 0.000000000000000000, 0.000000000000000000, -1.000000000000000000 ) ) ;
#25310=EDGE_LOOP ( 'NONE', ( #52070, #48630, #9275, #65539 ) ) ;
#25344=DIRECTION ( 'NONE',  ( -0.000000000000000000, 1.000000000000000000, -0.000000000000000000 ) ) ;
#25348=LINE ( 'NONE', #4486, #3418 ) ;
#25489=VECTOR ( 'NONE', #62350, 1000.000000000000000 ) ;
#25662=EDGE_LOOP ( 'NONE', ( #64477, #69476, #41115, #3181, #21579, #5829, #43014, #47381 ) ) ;
#25763=PRODUCT_CONTEXT ( 'NONE', #25050, 'mechanical' ) ;
#25918=DIRECTION ( 'NONE',  ( 0.000000000000000000, 1.000000000000000000, -0.000000000000000000 ) ) ;
#25985=VERTEX_POINT ( 'NONE', #52897 ) ;
#25998=CIRCLE ( 'NONE', #18189, 2.215251240775983899 ) ;
#26071=FACE_OUTER_BOUND ( 'NONE', #66738, .T. ) ;
#26107=SHAPE_DEFINITION_REPRESENTATION ( #66280, #62481 ) ;
#26410=CARTESIAN_POINT ( 'NONE',  ( 0.000000000000000000, 0.000000000000000000, 328.5239988703752942 ) ) ;
#26416=ORIENTED_EDGE ( 'NONE', *, *, #65712, .T. ) ;
#26623=VERTEX_POINT ( 'NONE', #19300 ) ;
#26762=DIRECTION ( 'NONE',  ( 0.000000000000000000, 1.000000000000000000, -0.000000000000000000 ) ) ;
#26813=DIRECTION ( 'NONE',  ( 0.000000000000000000, 0.000000000000000000, -1.000000000000000000 ) ) ;
#26863=PRODUCT_DEFINITION_FORMATION_WITH_SPECIFIED_SOURCE ( 'ANY', '', #37447, .NOT_KNOWN. ) ;
#26909=DIRECTION ( 'NONE',  ( 0.000000000000000000, 0.000000000000000000, 1.000000000000000000 ) ) ;
#27074=PLANE ( 'NONE',  #2897 ) ;
#27163=EDGE_CURVE ( 'NONE', #25985, #36828, #46443, .T. ) ;
#27176=CARTESIAN_POINT ( 'NONE',  ( 151.5599459900709860, -10.00000000000000178, 326.8892501111512843 ) ) ;
#27181=ADVANCED_FACE ( 'NONE', ( #13917 ), #63063, .F. ) ;
#27258=LINE ( 'NONE', #48825, #21037 ) ;
#27305=CARTESIAN_POINT ( 'NONE',  ( 151.5599459900709860, -10.00000000000000178, 322.4587476295993156 ) ) ;
#27337=EDGE_CURVE ( 'NONE', #65968, #25985, #28887, .T. ) ;
#27407=UNCERTAINTY_MEASURE_WITH_UNIT (LENGTH_MEASURE( 1.000000000000000082E-05 ), #64992, 'distance_accuracy_value', 'NONE');
#27534=CARTESIAN_POINT ( 'NONE',  ( 176.4833316329832940, 0.000000000000000000, 324.6739988703752715 ) ) ;
#27565=EDGE_LOOP ( 'NONE', ( #14895, #1170 ) ) ;
#27645=FACE_OUTER_BOUND ( 'NONE', #53309, .T. ) ;
#27773=CARTESIAN_POINT ( 'NONE',  ( 0.000000000000000000, 0.000000000000000000, 276.7801873289890295 ) ) ;
#27977=EDGE_LOOP ( 'NONE', ( #1221, #53217 ) ) ;
#28249=ORIENTED_EDGE ( 'NONE', *, *, #10920, .F. ) ;
#28256=AXIS2_PLACEMENT_3D ( 'NONE', #12170, #45384, #28775 ) ;
#28414=ADVANCED_BREP_SHAPE_REPRESENTATION ( '', ( #19304, #45918 ), #69670 ) ;
#28541=DIRECTION ( 'NONE',  ( 0.000000000000000000, 1.000000000000000000, 0.000000000000000000 ) ) ;
#28675=FACE_BOUND ( 'NONE', #58881, .T. ) ;
#28759=PRODUCT_DEFINITION ( 'UNKNOWN', '', #26863, #2065 ) ;
#28775=DIRECTION ( 'NONE',  ( -1.000000000000000000, 0.000000000000000000, -0.000000000000000000 ) ) ;
#28793=CARTESIAN_POINT ( 'NONE',  ( 176.4833316329832940, 0.000000000000000000, 282.8454385697650082 ) ) ;
#28887=CIRCLE ( 'NONE', #53765, 2.215251240775983899 ) ;
#29571=EDGE_LOOP ( 'NONE', ( #40795, #44761, #30264, #41459 ) ) ;
#29582=CARTESIAN_POINT ( 'NONE',  ( 181.4833316329832940, 0.000000000000000000, 328.5239988703752942 ) ) ;
#29606=ORIENTED_EDGE ( 'NONE', *, *, #24866, .F. ) ;
#29631=FACE_OUTER_BOUND ( 'NONE', #18567, .T. ) ;
#29932=CARTESIAN_POINT ( 'NONE',  ( 181.4833316329832940, 9.000000000000001776, 328.5239988703752942 ) ) ;
#29935=LINE ( 'NONE', #69174, #47804 ) ;
#30102=LINE ( 'NONE', #35751, #5801 ) ;
#30264=ORIENTED_EDGE ( 'NONE', *, *, #54809, .T. ) ;
#30305=CYLINDRICAL_SURFACE ( 'NONE', #13037, 2.215251240775983899 ) ;
#30313=VERTEX_POINT ( 'NONE', #19723 ) ;
#30406=ORIENTED_EDGE ( 'NONE', *, *, #39275, .T. ) ;
#30454=DIRECTION ( 'NONE',  ( 0.000000000000000000, 0.000000000000000000, 1.000000000000000000 ) ) ;
#30466=CARTESIAN_POINT ( 'NONE',  ( 176.4833316329832940, 0.000000000000000000, 280.6301873289890523 ) ) ;
#30549=CARTESIAN_POINT ( 'NONE',  ( 151.5599459900709860, 9.000000000000001776, 324.6739988703752715 ) ) ;
#30639=CARTESIAN_POINT ( 'NONE',  ( 151.5599459900709860, 9.000000000000001776, 324.6739988703752715 ) ) ;
#30647=DIRECTION ( 'NONE',  ( -0.000000000000000000, 1.000000000000000000, -0.000000000000000000 ) ) ;
#30923=CARTESIAN_POINT ( 'NONE',  ( 151.5599459900709860, 9.000000000000001776, 326.8892501111512843 ) ) ;
#31004=AXIS2_PLACEMENT_3D ( 'NONE', #59395, #49484, #43471 ) ;
#31195=ORIENTED_EDGE ( 'NONE', *, *, #41199, .F. ) ;
#31222=EDGE_LOOP ( 'NONE', ( #17167, #25036, #50226, #47017, #24335, #45784, #12084, #5341 ) ) ;
#31244=VERTEX_POINT ( 'NONE', #20316 ) ;
#31303=AXIS2_PLACEMENT_3D ( 'NONE', #59684, #22548, #44103 ) ;
#32355=DIRECTION ( 'NONE',  ( 1.000000000000000000, 0.000000000000000000, 0.000000000000000000 ) ) ;
#32473=CARTESIAN_POINT ( 'NONE',  ( 151.5599459900709860, 0.000000000000000000, 324.6739988703752715 ) ) ;
#32540=CYLINDRICAL_SURFACE ( 'NONE', #31004, 2.215251240775983899 ) ;
#32820=DIRECTION ( 'NONE',  ( 0.000000000000000000, 0.000000000000000000, 1.000000000000000000 ) ) ;
#33179=CARTESIAN_POINT ( 'NONE',  ( 181.4833316329832940, 9.000000000000001776, 320.8239988703753056 ) ) ;
#33185=VERTEX_POINT ( 'NONE', #2493 ) ;
#33204=AXIS2_PLACEMENT_3D ( 'NONE', #7323, #56818, #3094 ) ;
#33254=CARTESIAN_POINT ( 'NONE',  ( 181.4833316329832940, 9.000000000000001776, 276.7801873289890295 ) ) ;
#33364=VECTOR ( 'NONE', #66427, 1000.000000000000000 ) ;
#33462=CARTESIAN_POINT ( 'NONE',  ( 176.4833316329832940, -10.00000000000000178, 324.6739988703752715 ) ) ;
#33508=DIRECTION ( 'NONE',  ( -0.000000000000000000, 1.000000000000000000, -0.000000000000000000 ) ) ;
#33654=ORIENTED_EDGE ( 'NONE', *, *, #41406, .F. ) ;
#33742=VECTOR ( 'NONE', #6081, 1000.000000000000000 ) ;
#33969=CARTESIAN_POINT ( 'NONE',  ( 176.4833316329832940, 0.000000000000000000, 278.4149360882130395 ) ) ;
#34114=CARTESIAN_POINT ( 'NONE',  ( 151.5599459900709860, 0.000000000000000000, 326.8892501111512843 ) ) ;
#34267=ORIENTED_EDGE ( 'NONE', *, *, #40199, .T. ) ;
#34385=AXIS2_PLACEMENT_3D ( 'NONE', #42441, #5670, #10970 ) ;
#34512=VECTOR ( 'NONE', #49456, 1000.000000000000000 ) ;
#34757=CARTESIAN_POINT ( 'NONE',  ( 146.5599459900709860, 0.000000000000000000, 328.5239988703752942 ) ) ;
#34848=LINE ( 'NONE', #67033, #40684 ) ;
#35025=DIRECTION ( 'NONE',  ( 0.000000000000000000, 0.000000000000000000, 1.000000000000000000 ) ) ;
#35027=CARTESIAN_POINT ( 'NONE',  ( 176.4833316329832940, 0.000000000000000000, 280.6301873289890523 ) ) ;
#35208=VECTOR ( 'NONE', #8456, 1000.000000000000000 ) ;
#35326=EDGE_LOOP ( 'NONE', ( #6113, #16708, #7762, #35634 ) ) ;
#35327=EDGE_CURVE ( 'NONE', #48708, #37841, #52108, .T. ) ;
#35404=CARTESIAN_POINT ( 'NONE',  ( 146.5599459900709860, 9.000000000000001776, 284.4801873289890182 ) ) ;
#35634=ORIENTED_EDGE ( 'NONE', *, *, #44661, .T. ) ;
#35706=EDGE_CURVE ( 'NONE', #56861, #56386, #23366, .T. ) ;
#35735=CYLINDRICAL_SURFACE ( 'NONE', #23097, 2.215251240775983899 ) ;
#35751=CARTESIAN_POINT ( 'NONE',  ( 146.5599459900709860, 9.000000000000001776, 320.8239988703753056 ) ) ;
#36026=VECTOR ( 'NONE', #2538, 1000.000000000000000 ) ;
#36448=FACE_OUTER_BOUND ( 'NONE', #25662, .T. ) ;
#36483=LINE ( 'NONE', #7934, #11929 ) ;
#36750=VECTOR ( 'NONE', #305, 1000.000000000000000 ) ;
#36794=ORIENTED_EDGE ( 'NONE', *, *, #6881, .F. ) ;
#36828=VERTEX_POINT ( 'NONE', #12433 ) ;
#37178=DIRECTION ( 'NONE',  ( 1.000000000000000000, 0.000000000000000000, 0.000000000000000000 ) ) ;
#37179=ORIENTED_EDGE ( 'NONE', *, *, #16190, .T. ) ;
#37447=PRODUCT ( 'HOLDING PLATE', 'HOLDING PLATE', '', ( #25763 ) ) ;
#37625=CIRCLE ( 'NONE', #8215, 2.215251240775983899 ) ;
#37802=ORIENTED_EDGE ( 'NONE', *, *, #69483, .T. ) ;
#37803=DIRECTION ( 'NONE',  ( -1.000000000000000000, 0.000000000000000000, 0.000000000000000000 ) ) ;
#37841=VERTEX_POINT ( 'NONE', #48231 ) ;
#37911=ORIENTED_EDGE ( 'NONE', *, *, #7468, .T. ) ;
#37919=FACE_BOUND ( 'NONE', #27977, .T. ) ;
#37965=VECTOR ( 'NONE', #67776, 1000.000000000000000 ) ;
#38061=DIRECTION ( 'NONE',  ( 0.000000000000000000, -0.000000000000000000, -1.000000000000000000 ) ) ;
#38086=ORIENTED_EDGE ( 'NONE', *, *, #64646, .F. ) ;
#38330=VECTOR ( 'NONE', #6385, 1000.000000000000000 ) ;
#38346=CARTESIAN_POINT ( 'NONE',  ( 181.4833316329832940, 0.000000000000000000, 316.5239988703752942 ) ) ;
#38494=DIRECTION ( 'NONE',  ( 0.000000000000000000, -1.000000000000000000, 0.000000000000000000 ) ) ;
#38609=CARTESIAN_POINT ( 'NONE',  ( 146.5599459900709860, 9.000000000000001776, 324.5239988703752942 ) ) ;
#38824=FACE_OUTER_BOUND ( 'NONE', #31222, .T. ) ;
#39240=DIRECTION ( 'NONE',  ( 0.000000000000000000, 0.000000000000000000, -1.000000000000000000 ) ) ;
#39267=CARTESIAN_POINT ( 'NONE',  ( 151.5599459900709860, 0.000000000000000000, 322.4587476295993156 ) ) ;
#39271=EDGE_CURVE ( 'NONE', #19830, #58210, #2152, .T. ) ;
#39275=EDGE_CURVE ( 'NONE', #31244, #8538, #40727, .T. ) ;
#39761=DIRECTION ( 'NONE',  ( -0.000000000000000000, 1.000000000000000000, -0.000000000000000000 ) ) ;
#39907=VERTEX_POINT ( 'NONE', #1668 ) ;
#39962=AXIS2_PLACEMENT_3D ( 'NONE', #41814, #69387, #63747 ) ;
#39987=EDGE_CURVE ( 'NONE', #1391, #36828, #67763, .T. ) ;
#40199=EDGE_CURVE ( 'NONE', #41571, #66056, #25348, .T. ) ;
#40329=AXIS2_PLACEMENT_3D ( 'NONE', #54484, #43857, #39240 ) ;
#40392=DIRECTION ( 'NONE',  ( -0.000000000000000000, 1.000000000000000000, -0.000000000000000000 ) ) ;
#40476=LINE ( 'NONE', #56046, #10949 ) ;
#40684=VECTOR ( 'NONE', #61367, 1000.000000000000000 ) ;
#40727=LINE ( 'NONE', #35404, #36026 ) ;
#40795=ORIENTED_EDGE ( 'NONE', *, *, #24990, .F. ) ;
#40862=AXIS2_PLACEMENT_3D ( 'NONE', #33462, #22166, #22511 ) ;
#41012=CARTESIAN_POINT ( 'NONE',  ( 181.4833316329832940, 5.000000000000000000, 284.4801873289890182 ) ) ;
#41115=ORIENTED_EDGE ( 'NONE', *, *, #4428, .F. ) ;
#41199=EDGE_CURVE ( 'NONE', #56386, #56861, #7888, .T. ) ;
#41342=DIRECTION ( 'NONE',  ( 0.000000000000000000, -0.000000000000000000, 1.000000000000000000 ) ) ;
#41392=DIRECTION ( 'NONE',  ( -0.000000000000000000, 1.000000000000000000, -0.000000000000000000 ) ) ;
#41406=EDGE_CURVE ( 'NONE', #66056, #63673, #25998, .T. ) ;
#41459=ORIENTED_EDGE ( 'NONE', *, *, #22230, .T. ) ;
#41571=VERTEX_POINT ( 'NONE', #64937 ) ;
#41695=LINE ( 'NONE', #50897, #35208 ) ;
#41814=CARTESIAN_POINT ( 'NONE',  ( 151.5599459900709860, -10.00000000000000178, 324.6739988703752715 ) ) ;
#41872=CARTESIAN_POINT ( 'NONE',  ( 146.5599459900709860, 5.000000000000000000, 316.5239988703752942 ) ) ;
#41910=VECTOR ( 'NONE', #5156, 1000.000000000000000 ) ;
#42007=EDGE_CURVE ( 'NONE', #2806, #31244, #13483, .T. ) ;
#42041=LINE ( 'NONE', #16216, #36750 ) ;
#42107=CARTESIAN_POINT ( 'NONE',  ( 151.5599459900709860, 9.000000000000001776, 280.6301873289890523 ) ) ;
#42174=ORIENTED_EDGE ( 'NONE', *, *, #40199, .F. ) ;
#42218=LINE ( 'NONE', #41872, #60469 ) ;
#42265=ORIENTED_EDGE ( 'NONE', *, *, #27163, .T. ) ;
#42441=CARTESIAN_POINT ( 'NONE',  ( 151.5599459900709860, 0.000000000000000000, 280.6301873289890523 ) ) ;
#42451=AXIS2_PLACEMENT_3D ( 'NONE', #21653, #796, #43209 ) ;
#42544=DIRECTION ( 'NONE',  ( 0.000000000000000000, -1.000000000000000000, 0.000000000000000000 ) ) ;
#42629=EDGE_CURVE ( 'NONE', #45034, #48708, #30102, .T. ) ;
#42644=DIRECTION ( 'NONE',  ( 0.000000000000000000, 0.000000000000000000, -1.000000000000000000 ) ) ;
#42667=PLANE ( 'NONE',  #65003 ) ;
#42699=EDGE_LOOP ( 'NONE', ( #55538, #19747, #2682, #15502 ) ) ;
#43008=DIRECTION ( 'NONE',  ( 0.000000000000000000, 0.000000000000000000, -1.000000000000000000 ) ) ;
#43014=ORIENTED_EDGE ( 'NONE', *, *, #42007, .F. ) ;
#43094=PLANE ( 'NONE',  #53730 ) ;
#43209=DIRECTION ( 'NONE',  ( 0.000000000000000000, -0.000000000000000000, -1.000000000000000000 ) ) ;
#43471=DIRECTION ( 'NONE',  ( 0.000000000000000000, 0.000000000000000000, 1.000000000000000000 ) ) ;
#43487=DIRECTION ( 'NONE',  ( -0.000000000000000000, -1.000000000000000000, -0.000000000000000000 ) ) ;
#43523=ADVANCED_FACE ( 'NONE', ( #45317 ), #23425, .F. ) ;
#43605=LINE ( 'NONE', #16747, #15209 ) ;
#43857=DIRECTION ( 'NONE',  ( 0.000000000000000000, -1.000000000000000000, 0.000000000000000000 ) ) ;
#43900=PLANE ( 'NONE',  #42451 ) ;
#43902=LINE ( 'NONE', #38609, #14233 ) ;
#43922=CARTESIAN_POINT ( 'NONE',  ( 146.5599459900709860, 5.000000000000000000, 284.4801873289890182 ) ) ;
#44103=DIRECTION ( 'NONE',  ( 0.000000000000000000, -0.000000000000000000, -1.000000000000000000 ) ) ;
#44126=LINE ( 'NONE', #54415, #34512 ) ;
#44207=CARTESIAN_POINT ( 'NONE',  ( 181.4833316329832940, 5.000000000000000000, 320.8239988703753056 ) ) ;
#44462=CARTESIAN_POINT ( 'NONE',  ( 151.5599459900709860, 0.000000000000000000, 324.6739988703752715 ) ) ;
#44571=ORIENTED_EDGE ( 'NONE', *, *, #16936, .F. ) ;
#44661=EDGE_CURVE ( 'NONE', #8538, #37841, #42218, .T. ) ;
#44761=ORIENTED_EDGE ( 'NONE', *, *, #35706, .T. ) ;
#44850=CARTESIAN_POINT ( 'NONE',  ( 146.5599459900709860, 0.000000000000000000, 316.5239988703752942 ) ) ;
#44856=ADVANCED_FACE ( 'NONE', ( #68586 ), #45332, .F. ) ;
#44909=ORIENTED_EDGE ( 'NONE', *, *, #59660, .T. ) ;
#44942=EDGE_CURVE ( 'NONE', #31244, #39907, #44126, .T. ) ;
#45008=ADVANCED_FACE ( 'NONE', ( #38824 ), #43094, .F. ) ;
#45034=VERTEX_POINT ( 'NONE', #33179 ) ;
#45037=PLANE ( 'NONE',  #28256 ) ;
#45093=ORIENTED_EDGE ( 'NONE', *, *, #39271, .T. ) ;
#45303=ORIENTED_EDGE ( 'NONE', *, *, #10920, .T. ) ;
#45317=FACE_OUTER_BOUND ( 'NONE', #50638, .T. ) ;
#45332=CYLINDRICAL_SURFACE ( 'NONE', #1766, 2.215251240775983899 ) ;
#45384=DIRECTION ( 'NONE',  ( 0.000000000000000000, 0.000000000000000000, -1.000000000000000000 ) ) ;
#45395=ORIENTED_EDGE ( 'NONE', *, *, #64646, .T. ) ;
#45784=ORIENTED_EDGE ( 'NONE', *, *, #7688, .F. ) ;
#45918=AXIS2_PLACEMENT_3D ( 'NONE', #22775, #53934, #32355 ) ;
#45954=EDGE_CURVE ( 'NONE', #41571, #61801, #61776, .T. ) ;
#46033=DIRECTION ( 'NONE',  ( 0.000000000000000000, 0.000000000000000000, 1.000000000000000000 ) ) ;
#46050=CARTESIAN_POINT ( 'NONE',  ( 146.5599459900709860, 9.000000000000001776, 320.8239988703753056 ) ) ;
#46294=VECTOR ( 'NONE', #65989, 1000.000000000000000 ) ;
#46295=CARTESIAN_POINT ( 'NONE',  ( 0.000000000000000000, 9.000000000000001776, 0.000000000000000000 ) ) ;
#46443=LINE ( 'NONE', #3315, #25489 ) ;
#46543=EDGE_CURVE ( 'NONE', #30313, #33185, #23579, .T. ) ;
#47017=ORIENTED_EDGE ( 'NONE', *, *, #11954, .T. ) ;
#47381=ORIENTED_EDGE ( 'NONE', *, *, #55725, .F. ) ;
#47466=DIRECTION ( 'NONE',  ( 0.000000000000000000, 0.000000000000000000, -1.000000000000000000 ) ) ;
#47498=DIRECTION ( 'NONE',  ( 0.000000000000000000, 0.000000000000000000, 1.000000000000000000 ) ) ;
#47804=VECTOR ( 'NONE', #25344, 1000.000000000000000 ) ;
#47933=CARTESIAN_POINT ( 'NONE',  ( 181.4833316329832940, 0.000000000000000000, 276.7801873289890295 ) ) ;
#48104=AXIS2_PLACEMENT_3D ( 'NONE', #51397, #57049, #47498 ) ;
#48231=CARTESIAN_POINT ( 'NONE',  ( 146.5599459900709860, 5.000000000000000000, 320.8239988703753056 ) ) ;
#48352=DIRECTION ( 'NONE',  ( 1.000000000000000000, 0.000000000000000000, 0.000000000000000000 ) ) ;
#48628=UNCERTAINTY_MEASURE_WITH_UNIT (LENGTH_MEASURE( 1.000000000000000082E-05 ), #184, 'distance_accuracy_value', 'NONE');
#48630=ORIENTED_EDGE ( 'NONE', *, *, #44942, .T. ) ;
#48659=FACE_BOUND ( 'NONE', #6234, .T. ) ;
#48708=VERTEX_POINT ( 'NONE', #46050 ) ;
#48725=PLANE ( 'NONE',  #31303 ) ;
#48825=CARTESIAN_POINT ( 'NONE',  ( 146.5599459900709860, 0.000000000000000000, 328.5239988703752942 ) ) ;
#48992=ORIENTED_EDGE ( 'NONE', *, *, #12728, .T. ) ;
#48996=FACE_OUTER_BOUND ( 'NONE', #4798, .T. ) ;
#49034=CYLINDRICAL_SURFACE ( 'NONE', #40862, 2.215251240775983899 ) ;
#49415=ORIENTED_EDGE ( 'NONE', *, *, #62598, .T. ) ;
#49456=DIRECTION ( 'NONE',  ( 1.000000000000000000, 0.000000000000000000, 0.000000000000000000 ) ) ;
#49484=DIRECTION ( 'NONE',  ( -0.000000000000000000, 1.000000000000000000, -0.000000000000000000 ) ) ;
#49770=ORIENTED_EDGE ( 'NONE', *, *, #7751, .T. ) ;
#49821=DIRECTION ( 'NONE',  ( -0.000000000000000000, 1.000000000000000000, -0.000000000000000000 ) ) ;
#50226=ORIENTED_EDGE ( 'NONE', *, *, #23032, .F. ) ;
#50638=EDGE_LOOP ( 'NONE', ( #48992, #24554, #65917, #8432 ) ) ;
#50801=EDGE_LOOP ( 'NONE', ( #68152, #1054 ) ) ;
#50807=DIRECTION ( 'NONE',  ( -0.000000000000000000, 1.000000000000000000, -0.000000000000000000 ) ) ;
#50897=CARTESIAN_POINT ( 'NONE',  ( 146.5599459900709860, 0.000000000000000000, 276.7801873289890295 ) ) ;
#50983=DIRECTION ( 'NONE',  ( 0.000000000000000000, 0.000000000000000000, -1.000000000000000000 ) ) ;
#51204=CYLINDRICAL_SURFACE ( 'NONE', #11623, 2.215251240775983899 ) ;
#51397=CARTESIAN_POINT ( 'NONE',  ( 151.5599459900709860, -10.00000000000000178, 280.6301873289890523 ) ) ;
#51412=CARTESIAN_POINT ( 'NONE',  ( 176.4833316329832940, 9.000000000000001776, 280.6301873289890523 ) ) ;
#51519=LINE ( 'NONE', #57169, #37965 ) ;
#51828=ADVANCED_FACE ( 'NONE', ( #65306 ), #49034, .F. ) ;
#51965=CARTESIAN_POINT ( 'NONE',  ( 151.5599459900709860, 9.000000000000001776, 322.4587476295993156 ) ) ;
#52070=ORIENTED_EDGE ( 'NONE', *, *, #42007, .T. ) ;
#52108=LINE ( 'NONE', #57406, #1866 ) ;
#52188=LINE ( 'NONE', #47933, #41910 ) ;
#52301=VECTOR ( 'NONE', #24991, 1000.000000000000000 ) ;
#52416=ORIENTED_EDGE ( 'NONE', *, *, #13074, .F. ) ;
#52570=ADVANCED_FACE ( 'NONE', ( #57727 ), #20250, .F. ) ;
#52752=STYLED_ITEM ( 'NONE', ( #6279 ), #19304 ) ;
#52811=VECTOR ( 'NONE', #13161, 1000.000000000000000 ) ;
#52897=CARTESIAN_POINT ( 'NONE',  ( 151.5599459900709860, 0.000000000000000000, 282.8454385697650082 ) ) ;
#52952=VERTEX_POINT ( 'NONE', #62962 ) ;
#53061=ADVANCED_FACE ( 'NONE', ( #59048 ), #32540, .F. ) ;
#53217=ORIENTED_EDGE ( 'NONE', *, *, #27337, .F. ) ;
#53309=EDGE_LOOP ( 'NONE', ( #65292, #1289, #14599, #36794 ) ) ;
#53318=LINE ( 'NONE', #57905, #64129 ) ;
#53460=ORIENTED_EDGE ( 'NONE', *, *, #41199, .T. ) ;
#53672=EDGE_CURVE ( 'NONE', #1231, #52952, #62070, .T. ) ;
#53730=AXIS2_PLACEMENT_3D ( 'NONE', #60383, #37803, #59365 ) ;
#53734=ORIENTED_EDGE ( 'NONE', *, *, #15089, .T. ) ;
#53757=ORIENTED_EDGE ( 'NONE', *, *, #45954, .F. ) ;
#53765=AXIS2_PLACEMENT_3D ( 'NONE', #20970, #42544, #64815 ) ;
#53934=DIRECTION ( 'NONE',  ( 0.000000000000000000, 0.000000000000000000, 1.000000000000000000 ) ) ;
#53973=FACE_BOUND ( 'NONE', #61226, .T. ) ;
#54084=VERTEX_POINT ( 'NONE', #63348 ) ;
#54415=CARTESIAN_POINT ( 'NONE',  ( 146.5599459900709860, 9.000000000000001776, 284.4801873289890182 ) ) ;
#54484=CARTESIAN_POINT ( 'NONE',  ( 176.4833316329832940, 0.000000000000000000, 324.6739988703752715 ) ) ;
#54809=EDGE_CURVE ( 'NONE', #56386, #3052, #65350, .T. ) ;
#55448=DIRECTION ( 'NONE',  ( 0.000000000000000000, 0.000000000000000000, -1.000000000000000000 ) ) ;
#55538=ORIENTED_EDGE ( 'NONE', *, *, #4428, .T. ) ;
#55725=EDGE_CURVE ( 'NONE', #17940, #2806, #41695, .T. ) ;
#55752=ADVANCED_FACE ( 'NONE', ( #56896, #13771, #3177 ), #14485, .T. ) ;
#55962=ORIENTED_EDGE ( 'NONE', *, *, #16936, .T. ) ;
#56046=CARTESIAN_POINT ( 'NONE',  ( 181.4833316329832940, 9.000000000000001776, 280.7801873289890295 ) ) ;
#56060=CIRCLE ( 'NONE', #2967, 2.215251240775983899 ) ;
#56118=DIRECTION ( 'NONE',  ( -1.000000000000000000, 0.000000000000000000, 0.000000000000000000 ) ) ;
#56386=VERTEX_POINT ( 'NONE', #34114 ) ;
#56522=ORIENTED_EDGE ( 'NONE', *, *, #27163, .F. ) ;
#56796=EDGE_LOOP ( 'NONE', ( #17443, #26416, #34267, #6931 ) ) ;
#56818=DIRECTION ( 'NONE',  ( 0.000000000000000000, 1.000000000000000000, 0.000000000000000000 ) ) ;
#56861=VERTEX_POINT ( 'NONE', #39267 ) ;
#56894=ORIENTED_EDGE ( 'NONE', *, *, #24866, .T. ) ;
#56896=FACE_BOUND ( 'NONE', #20007, .T. ) ;
#56925=CARTESIAN_POINT ( 'NONE',  ( 176.4833316329832940, 9.000000000000001776, 278.4149360882130395 ) ) ;
#57049=DIRECTION ( 'NONE',  ( -0.000000000000000000, 1.000000000000000000, -0.000000000000000000 ) ) ;
#57169=CARTESIAN_POINT ( 'NONE',  ( 151.5599459900709860, -10.00000000000000178, 278.4149360882130395 ) ) ;
#57406=CARTESIAN_POINT ( 'NONE',  ( 146.5599459900709860, 9.000000000000001776, 320.8239988703753056 ) ) ;
#57586=EDGE_LOOP ( 'NONE', ( #45093, #45395, #7481, #68608 ) ) ;
#57727=FACE_OUTER_BOUND ( 'NONE', #20705, .T. ) ;
#57905=CARTESIAN_POINT ( 'NONE',  ( 146.5599459900709860, 5.000000000000000000, 284.4801873289890182 ) ) ;
#57926=ORIENTED_EDGE ( 'NONE', *, *, #24990, .T. ) ;
#58018=CARTESIAN_POINT ( 'NONE',  ( 146.5599459900709860, 5.000000000000000000, 316.5239988703752942 ) ) ;
#58210=VERTEX_POINT ( 'NONE', #33969 ) ;
#58211=DIRECTION ( 'NONE',  ( 0.000000000000000000, 1.000000000000000000, -0.000000000000000000 ) ) ;
#58881=EDGE_LOOP ( 'NONE', ( #53757, #17040 ) ) ;
#59048=FACE_OUTER_BOUND ( 'NONE', #57586, .T. ) ;
#59365=DIRECTION ( 'NONE',  ( 0.000000000000000000, 0.000000000000000000, 1.000000000000000000 ) ) ;
#59395=CARTESIAN_POINT ( 'NONE',  ( 176.4833316329832940, -10.00000000000000178, 280.6301873289890523 ) ) ;
#59530=ADVANCED_FACE ( 'NONE', ( #4286 ), #35735, .F. ) ;
#59660=EDGE_CURVE ( 'NONE', #25985, #65968, #11835, .T. ) ;
#59684=CARTESIAN_POINT ( 'NONE',  ( 0.000000000000000000, 5.000000000000000000, 0.000000000000000000 ) ) ;
#59771=VERTEX_POINT ( 'NONE', #65410 ) ;
#59932=DIRECTION ( 'NONE',  ( 1.000000000000000000, 0.000000000000000000, 0.000000000000000000 ) ) ;
#60383=CARTESIAN_POINT ( 'NONE',  ( 181.4833316329832940, 5.000000000000000000, 316.5239988703752942 ) ) ;
#60469=VECTOR ( 'NONE', #64500, 1000.000000000000000 ) ;
#60477=ORIENTED_EDGE ( 'NONE', *, *, #54809, .F. ) ;
#60609=ORIENTED_EDGE ( 'NONE', *, *, #39987, .T. ) ;
#60692=EDGE_LOOP ( 'NONE', ( #52416, #64489, #42265, #49415 ) ) ;
#60734=DIRECTION ( 'NONE',  ( 0.000000000000000000, 0.000000000000000000, -1.000000000000000000 ) ) ;
#61043=FILL_AREA_STYLE_COLOUR ( '', #18850 ) ;
#61226=EDGE_LOOP ( 'NONE', ( #12956, #28249 ) ) ;
#61367=DIRECTION ( 'NONE',  ( 0.000000000000000000, 0.000000000000000000, -1.000000000000000000 ) ) ;
#61776=CIRCLE ( 'NONE', #40329, 2.215251240775983899 ) ;
#61801=VERTEX_POINT ( 'NONE', #66284 ) ;
#61802=EDGE_CURVE ( 'NONE', #2806, #26623, #11825, .T. ) ;
#62070=CIRCLE ( 'NONE', #62114, 2.215251240775983899 ) ;
#62110=FACE_OUTER_BOUND ( 'NONE', #29571, .T. ) ;
#62114=AXIS2_PLACEMENT_3D ( 'NONE', #51412, #67680, #8269 ) ;
#62350=DIRECTION ( 'NONE',  ( -0.000000000000000000, 1.000000000000000000, -0.000000000000000000 ) ) ;
#62481=SHAPE_REPRESENTATION ( 'HOLDING PLATE', ( #45918 ), #69670 ) ;
#62598=EDGE_CURVE ( 'NONE', #36828, #1391, #8663, .T. ) ;
#62645=CARTESIAN_POINT ( 'NONE',  ( 146.5599459900709860, 9.000000000000001776, 328.5239988703752942 ) ) ;
#62962=CARTESIAN_POINT ( 'NONE',  ( 176.4833316329832940, 9.000000000000001776, 282.8454385697650082 ) ) ;
#62976=ORIENTED_EDGE ( 'NONE', *, *, #35706, .F. ) ;
#63063=CYLINDRICAL_SURFACE ( 'NONE', #48104, 2.215251240775983899 ) ;
#63348=CARTESIAN_POINT ( 'NONE',  ( 181.4833316329832940, 0.000000000000000000, 276.7801873289890295 ) ) ;
#63673=VERTEX_POINT ( 'NONE', #13848 ) ;
#63747=DIRECTION ( 'NONE',  ( 0.000000000000000000, 0.000000000000000000, 1.000000000000000000 ) ) ;
#63993=EDGE_CURVE ( 'NONE', #26623, #54084, #11668, .T. ) ;
#64016=ORIENTED_EDGE ( 'NONE', *, *, #44942, .F. ) ;
#64129=VECTOR ( 'NONE', #48352, 1000.000000000000000 ) ;
#64156=DIRECTION ( 'NONE',  ( -0.000000000000000000, -1.000000000000000000, -0.000000000000000000 ) ) ;
#64477=ORIENTED_EDGE ( 'NONE', *, *, #4982, .T. ) ;
#64489=ORIENTED_EDGE ( 'NONE', *, *, #27337, .T. ) ;
#64500=DIRECTION ( 'NONE',  ( -0.000000000000000000, -0.000000000000000000, 1.000000000000000000 ) ) ;
#64622=EDGE_CURVE ( 'NONE', #59771, #30313, #8009, .T. ) ;
#64646=EDGE_CURVE ( 'NONE', #58210, #1231, #29935, .T. ) ;
#64814=APPLICATION_CONTEXT ( 'automotive_design' ) ;
#64815=DIRECTION ( 'NONE',  ( 0.000000000000000000, 0.000000000000000000, -1.000000000000000000 ) ) ;
#64883=( NAMED_UNIT ( * ) PLANE_ANGLE_UNIT ( ) SI_UNIT ( $, .RADIAN. ) );
#64937=CARTESIAN_POINT ( 'NONE',  ( 176.4833316329832940, 0.000000000000000000, 326.8892501111512843 ) ) ;
#64989=DIRECTION ( 'NONE',  ( 0.000000000000000000, 0.000000000000000000, -1.000000000000000000 ) ) ;
#64992=( LENGTH_UNIT ( ) NAMED_UNIT ( * ) SI_UNIT ( .MILLI., .METRE. ) );
#65003=AXIS2_PLACEMENT_3D ( 'NONE', #26410, #69192, #20747 ) ;
#65292=ORIENTED_EDGE ( 'NONE', *, *, #67397, .F. ) ;
#65306=FACE_OUTER_BOUND ( 'NONE', #2742, .T. ) ;
#65350=LINE ( 'NONE', #27176, #66714 ) ;
#65410=CARTESIAN_POINT ( 'NONE',  ( 181.4833316329832940, 0.000000000000000000, 328.5239988703752942 ) ) ;
#65539=ORIENTED_EDGE ( 'NONE', *, *, #61802, .F. ) ;
#65712=EDGE_CURVE ( 'NONE', #61801, #41571, #37625, .T. ) ;
#65917=ORIENTED_EDGE ( 'NONE', *, *, #42629, .F. ) ;
#65968=VERTEX_POINT ( 'NONE', #16499 ) ;
#65989=DIRECTION ( 'NONE',  ( -0.000000000000000000, 1.000000000000000000, -0.000000000000000000 ) ) ;
#66007=SURFACE_STYLE_USAGE ( .BOTH. , #12255 ) ;
#66056=VERTEX_POINT ( 'NONE', #17179 ) ;
#66115=EDGE_LOOP ( 'NONE', ( #44909, #14224, #60609, #56522 ) ) ;
#66208=ORIENTED_EDGE ( 'NONE', *, *, #46543, .T. ) ;
#66280=PRODUCT_DEFINITION_SHAPE ( 'NONE', 'NONE',  #28759 ) ;
#66284=CARTESIAN_POINT ( 'NONE',  ( 176.4833316329832940, 0.000000000000000000, 322.4587476295993156 ) ) ;
#66350=AXIS2_PLACEMENT_3D ( 'NONE', #22486, #21432, #38061 ) ;
#66427=DIRECTION ( 'NONE',  ( -0.000000000000000000, -0.000000000000000000, 1.000000000000000000 ) ) ;
#66429=CARTESIAN_POINT ( 'NONE',  ( 176.4833316329832940, -10.00000000000000178, 280.6301873289890523 ) ) ;
#66502=AXIS2_PLACEMENT_3D ( 'NONE', #30466, #8895, #50983 ) ;
#66551=DIRECTION ( 'NONE',  ( 1.000000000000000000, 0.000000000000000000, -0.000000000000000000 ) ) ;
#66714=VECTOR ( 'NONE', #33508, 1000.000000000000000 ) ;
#66738=EDGE_LOOP ( 'NONE', ( #66208, #37179, #53734, #23265 ) ) ;
#67033=CARTESIAN_POINT ( 'NONE',  ( 181.4833316329832940, 5.000000000000000000, 316.5239988703752942 ) ) ;
#67307=EDGE_LOOP ( 'NONE', ( #37802, #9324, #64016, #30406 ) ) ;
#67397=EDGE_CURVE ( 'NONE', #59771, #54084, #21030, .T. ) ;
#67565=VERTEX_POINT ( 'NONE', #34757 ) ;
#67579=ORIENTED_EDGE ( 'NONE', *, *, #53672, .F. ) ;
#67680=DIRECTION ( 'NONE',  ( 0.000000000000000000, 1.000000000000000000, 0.000000000000000000 ) ) ;
#67763=CIRCLE ( 'NONE', #11288, 2.215251240775983899 ) ;
#67776=DIRECTION ( 'NONE',  ( -0.000000000000000000, 1.000000000000000000, -0.000000000000000000 ) ) ;
#67806=ADVANCED_FACE ( 'NONE', ( #7096, #28675, #11037, #37919, #27645 ), #43900, .T. ) ;
#68152=ORIENTED_EDGE ( 'NONE', *, *, #62598, .F. ) ;
#68586=FACE_OUTER_BOUND ( 'NONE', #56796, .T. ) ;
#68608=ORIENTED_EDGE ( 'NONE', *, *, #7751, .F. ) ;
#68787=AXIS2_PLACEMENT_3D ( 'NONE', #15299, #25918, #47466 ) ;
#68892=LINE ( 'NONE', #20790, #11375 ) ;
#69174=CARTESIAN_POINT ( 'NONE',  ( 176.4833316329832940, -10.00000000000000178, 278.4149360882130395 ) ) ;
#69192=DIRECTION ( 'NONE',  ( 0.000000000000000000, 0.000000000000000000, 1.000000000000000000 ) ) ;
#69387=DIRECTION ( 'NONE',  ( -0.000000000000000000, 1.000000000000000000, -0.000000000000000000 ) ) ;
#69410=AXIS2_PLACEMENT_3D ( 'NONE', #30639, #58211, #42644 ) ;
#69476=ORIENTED_EDGE ( 'NONE', *, *, #16190, .F. ) ;
#69483=EDGE_CURVE ( 'NONE', #8538, #1200, #53318, .T. ) ;
#69541=CARTESIAN_POINT ( 'NONE',  ( 176.4833316329832940, 9.000000000000001776, 324.6739988703752715 ) ) ;
#69670=( GEOMETRIC_REPRESENTATION_CONTEXT ( 3 ) GLOBAL_UNCERTAINTY_ASSIGNED_CONTEXT ( ( #48628 ) ) GLOBAL_UNIT_ASSIGNED_CONTEXT ( ( #184, #64883, #12159 ) ) REPRESENTATION_CONTEXT ( 'NONE', 'WORKASPACE' ) );
#69692=DIRECTION ( 'NONE',  ( 1.000000000000000000, -0.000000000000000000, 0.000000000000000000 ) ) ;
ENDSEC;
END-ISO-10303-21;
